ISO-10303-21;
HEADER;
FILE_DESCRIPTION((''),'2;1');
FILE_NAME('Washer.step','2026-10-09T12:47:58-07:00',(''),(''),'','','');
FILE_SCHEMA (('AUTOMOTIVE_DESIGN { 1 0 10303 214 3 1 1 }'));
ENDSEC;
DATA;
#10=MECHANICAL_DESIGN_GEOMETRIC_PRESENTATION_REPRESENTATION('',(#319),#3475);
#159=FACE_BOUND('',#538,.T.) ;
#160=FACE_BOUND('',#540,.T.) ;
#207=CIRCLE('',#2104,4.5) ;
#208=CIRCLE('',#2105,4.5) ;
#209=CIRCLE('',#2107,25.) ;
#210=CIRCLE('',#2108,25.) ;
#276=CYLINDRICAL_SURFACE('',#2103,4.5) ;
#277=CYLINDRICAL_SURFACE('',#2106,25.) ;
#295=SHAPE_REPRESENTATION_RELATIONSHIP('SRR','None',#3551,#307) ;
#307=ADVANCED_BREP_SHAPE_REPRESENTATION('',(#331),#3471) ;
#319=STYLED_ITEM('',(#3628),#331) ;
#331=MANIFOLD_SOLID_BREP('Body1',#1833) ;
#403=FACE_OUTER_BOUND('',#535,.T.) ;
#404=FACE_OUTER_BOUND('',#536,.T.) ;
#405=FACE_OUTER_BOUND('',#537,.T.) ;
#406=FACE_OUTER_BOUND('',#539,.T.) ;
#535=EDGE_LOOP('',(#1464,#1465,#1466,#1467)) ;
#536=EDGE_LOOP('',(#1468,#1469,#1470,#1471)) ;
#537=EDGE_LOOP('',(#1472)) ;
#538=EDGE_LOOP('',(#1473)) ;
#539=EDGE_LOOP('',(#1474)) ;
#540=EDGE_LOOP('',(#1475)) ;
#677=LINE('',#3214,#796) ;
#678=LINE('',#3220,#797) ;
#796=VECTOR('',#2576,4.5) ;
#797=VECTOR('',#2583,25.) ;
#915=VERTEX_POINT('',#3211) ;
#916=VERTEX_POINT('',#3213) ;
#917=VERTEX_POINT('',#3217) ;
#918=VERTEX_POINT('',#3219) ;
#1104=EDGE_CURVE('',#915,#915,#207,.T.) ;
#1105=EDGE_CURVE('',#915,#916,#677,.T.) ;
#1106=EDGE_CURVE('',#916,#916,#208,.T.) ;
#1107=EDGE_CURVE('',#917,#917,#209,.T.) ;
#1108=EDGE_CURVE('',#917,#918,#678,.T.) ;
#1109=EDGE_CURVE('',#918,#918,#210,.T.) ;
#1464=ORIENTED_EDGE('',*,*,#1104,.T.) ;
#1465=ORIENTED_EDGE('',*,*,#1105,.T.) ;
#1466=ORIENTED_EDGE('',*,*,#1106,.F.) ;
#1467=ORIENTED_EDGE('',*,*,#1105,.F.) ;
#1468=ORIENTED_EDGE('',*,*,#1107,.T.) ;
#1469=ORIENTED_EDGE('',*,*,#1108,.T.) ;
#1470=ORIENTED_EDGE('',*,*,#1109,.F.) ;
#1471=ORIENTED_EDGE('',*,*,#1108,.F.) ;
#1472=ORIENTED_EDGE('',*,*,#1109,.T.) ;
#1473=ORIENTED_EDGE('',*,*,#1104,.F.) ;
#1474=ORIENTED_EDGE('',*,*,#1107,.F.) ;
#1475=ORIENTED_EDGE('',*,*,#1106,.T.) ;
#1689=PLANE('',#2109) ;
#1690=PLANE('',#2110) ;
#1779=ADVANCED_FACE('',(#403),#276,.F.) ;
#1780=ADVANCED_FACE('',(#404),#277,.T.) ;
#1781=ADVANCED_FACE('',(#405,#159),#1689,.T.) ;
#1782=ADVANCED_FACE('',(#406,#160),#1690,.F.) ;
#1833=CLOSED_SHELL('',(#1779,#1780,#1781,#1782)) ;
#2102=AXIS2_PLACEMENT_3D('',#3209,#2570,#2571) ;
#2103=AXIS2_PLACEMENT_3D('',#3210,#2572,#2573) ;
#2104=AXIS2_PLACEMENT_3D('',#3212,#2574,#2575) ;
#2105=AXIS2_PLACEMENT_3D('',#3215,#2577,#2578) ;
#2106=AXIS2_PLACEMENT_3D('',#3216,#2579,#2580) ;
#2107=AXIS2_PLACEMENT_3D('',#3218,#2581,#2582) ;
#2108=AXIS2_PLACEMENT_3D('',#3221,#2584,#2585) ;
#2109=AXIS2_PLACEMENT_3D('',#3222,#2586,#2587) ;
#2110=AXIS2_PLACEMENT_3D('',#3223,#2588,#2589) ;
#2570=DIRECTION('axis',(0.,0.,1.)) ;
#2571=DIRECTION('refdir',(1.,0.,0.)) ;
#2572=DIRECTION('center_axis',(-1.,0.,0.)) ;
#2573=DIRECTION('ref_axis',(0.,0.,1.)) ;
#2574=DIRECTION('center_axis',(1.,0.,0.)) ;
#2575=DIRECTION('ref_axis',(0.,0.,-1.)) ;
#2576=DIRECTION('',(-1.,0.,0.)) ;
#2577=DIRECTION('center_axis',(1.,0.,0.)) ;
#2578=DIRECTION('ref_axis',(0.,0.,-1.)) ;
#2579=DIRECTION('center_axis',(-1.,0.,0.)) ;
#2580=DIRECTION('ref_axis',(0.,0.,1.)) ;
#2581=DIRECTION('center_axis',(1.,0.,0.)) ;
#2582=DIRECTION('ref_axis',(0.,0.,-1.)) ;
#2583=DIRECTION('',(1.,0.,0.)) ;
#2584=DIRECTION('center_axis',(1.,0.,0.)) ;
#2585=DIRECTION('ref_axis',(0.,0.,-1.)) ;
#2586=DIRECTION('center_axis',(1.,0.,0.)) ;
#2587=DIRECTION('ref_axis',(0.,0.,-1.)) ;
#2588=DIRECTION('center_axis',(1.,0.,0.)) ;
#2589=DIRECTION('ref_axis',(0.,0.,-1.)) ;
#3209=CARTESIAN_POINT('',(0.,0.,0.)) ;
#3210=CARTESIAN_POINT('Origin',(5.,0.,0.)) ;
#3211=CARTESIAN_POINT('',(5.,-5.51091059616309E-16,-4.5)) ;
#3212=CARTESIAN_POINT('Origin',(5.,0.,0.)) ;
#3213=CARTESIAN_POINT('',(0.,-5.51091059616309E-16,-4.5)) ;
#3214=CARTESIAN_POINT('',(5.,-5.51091059616309E-16,-4.5)) ;
#3215=CARTESIAN_POINT('Origin',(0.,0.,0.)) ;
#3216=CARTESIAN_POINT('Origin',(5.,0.,0.)) ;
#3217=CARTESIAN_POINT('',(0.,-3.06161699786838E-15,-25.)) ;
#3218=CARTESIAN_POINT('Origin',(0.,0.,0.)) ;
#3219=CARTESIAN_POINT('',(5.,-3.06161699786838E-15,-25.)) ;
#3220=CARTESIAN_POINT('',(5.,-3.06161699786838E-15,-25.)) ;
#3221=CARTESIAN_POINT('Origin',(5.,0.,0.)) ;
#3222=CARTESIAN_POINT('Origin',(5.,0.,0.)) ;
#3223=CARTESIAN_POINT('Origin',(0.,0.,0.)) ;
#3453=UNCERTAINTY_MEASURE_WITH_UNIT(LENGTH_MEASURE(0.01),#3476,
'DISTANCE_ACCURACY_VALUE',
'Maximum model space distance between geometric entities at asserted c
onnectivities') ;
#3457=UNCERTAINTY_MEASURE_WITH_UNIT(LENGTH_MEASURE(0.01),#3476,
'DISTANCE_ACCURACY_VALUE',
'Maximum model space distance between geometric entities at asserted c
onnectivities') ;
#3471=(
GEOMETRIC_REPRESENTATION_CONTEXT(3)
GLOBAL_UNCERTAINTY_ASSIGNED_CONTEXT((#3453))
GLOBAL_UNIT_ASSIGNED_CONTEXT((#3476,#3478,#3479))
REPRESENTATION_CONTEXT('','3D')
) ;
#3475=(
GEOMETRIC_REPRESENTATION_CONTEXT(3)
GLOBAL_UNCERTAINTY_ASSIGNED_CONTEXT((#3457))
GLOBAL_UNIT_ASSIGNED_CONTEXT((#3476,#3478,#3479))
REPRESENTATION_CONTEXT('','3D')
) ;
#3476=(
LENGTH_UNIT()
NAMED_UNIT(*)
SI_UNIT(.MILLI.,.METRE.)
) ;
#3478=(
NAMED_UNIT(*)
PLANE_ANGLE_UNIT()
SI_UNIT($,.RADIAN.)
) ;
#3479=(
NAMED_UNIT(*)
SI_UNIT($,.STERADIAN.)
SOLID_ANGLE_UNIT()
) ;
#3493=SHAPE_DEFINITION_REPRESENTATION(#3520,#3551) ;
#3520=PRODUCT_DEFINITION_SHAPE('',$,#3569) ;
#3551=SHAPE_REPRESENTATION('',(#2102),#3471) ;
#3555=PRODUCT_DEFINITION_CONTEXT('part definition',#3608,'design') ;
#3569=PRODUCT_DEFINITION('Washer',
'Washer',#3586,#3555) ;
#3586=PRODUCT_DEFINITION_FORMATION('',$,#3623) ;
#3608=APPLICATION_CONTEXT(
'Core Data for Automotive Mechanical Design Process') ;
#3609=PRODUCT_CONTEXT('part definition',#3608,'mechanical') ;
#3623=PRODUCT('Washer','Washer',$,(#3609)) ;
#3628=PRESENTATION_STYLE_ASSIGNMENT((#3630)) ;
#3630=SURFACE_STYLE_USAGE(.BOTH.,#3632) ;
#3632=SURFACE_SIDE_STYLE('',(#3634)) ;
#3634=SURFACE_STYLE_FILL_AREA(#3636) ;
#3636=FILL_AREA_STYLE('Opaque(202,209,238)',(#3638)) ;
#3638=FILL_AREA_STYLE_COLOUR('Opaque(202,209,238)',#3640) ;
#3640=COLOUR_RGB('Opaque(202,209,238)', 0.09019608, 0.27058824, 0.51372549) ;
ENDSEC;
END-ISO-10303-21;
